ISO-10303-21;
HEADER;
/* Generated by software containing ST-Developer
 * from STEP Tools, Inc. (www.steptools.com) 
 */

FILE_DESCRIPTION(
/* description */ ('Turntable on roller ring'),
/* implementation_level */ '2;1');

FILE_NAME(
/* name */ 'Roller axle (3).step',
/* time_stamp */ '2026-10-28T03:23:59-07:00',
/* author */ (''),
/* organization */ (''),
/* preprocessor_version */ 'ST-DEVELOPER v20.2',
/* originating_system */ 'Autodesk Translation Framework v15.17.0.0',
/* authorisation */ '');

FILE_SCHEMA (('AUTOMOTIVE_DESIGN { 1 0 10303 214 3 1 1 }'));
ENDSEC;

DATA;
#10=MECHANICAL_DESIGN_GEOMETRIC_PRESENTATION_REPRESENTATION('',(#658),#16281);
#539=SHAPE_REPRESENTATION_RELATIONSHIP('SRR','None',#16559,#594);
#594=ADVANCED_BREP_SHAPE_REPRESENTATION('',(#728),#16253);
#658=STYLED_ITEM('',(#16932),#728);
#728=MANIFOLD_SOLID_BREP('Body1',#8401);
#947=FACE_BOUND('',#2303,.T.);
#948=FACE_BOUND('',#2308,.T.);
#1177=PLANE('',#9803);
#1178=PLANE('',#9804);
#1179=PLANE('',#9809);
#1180=PLANE('',#9812);
#1605=FACE_OUTER_BOUND('',#2300,.T.);
#1606=FACE_OUTER_BOUND('',#2301,.T.);
#1607=FACE_OUTER_BOUND('',#2302,.T.);
#1608=FACE_OUTER_BOUND('',#2304,.T.);
#1609=FACE_OUTER_BOUND('',#2305,.T.);
#1610=FACE_OUTER_BOUND('',#2306,.T.);
#1611=FACE_OUTER_BOUND('',#2307,.T.);
#2300=EDGE_LOOP('',(#7139,#7140,#7141,#7142));
#2301=EDGE_LOOP('',(#7143));
#2302=EDGE_LOOP('',(#7144));
#2303=EDGE_LOOP('',(#7145));
#2304=EDGE_LOOP('',(#7146,#7147,#7148,#7149));
#2305=EDGE_LOOP('',(#7150));
#2306=EDGE_LOOP('',(#7151,#7152,#7153,#7154));
#2307=EDGE_LOOP('',(#7155));
#2308=EDGE_LOOP('',(#7156));
#2881=LINE('',#15113,#3364);
#2882=LINE('',#15123,#3365);
#2883=LINE('',#15129,#3366);
#3364=VECTOR('',#12112,0.165);
#3365=VECTOR('',#12125,0.8);
#3366=VECTOR('',#12134,0.5);
#3797=CIRCLE('',#9801,0.165);
#3798=CIRCLE('',#9802,0.165);
#3799=CIRCLE('',#9805,0.8);
#3800=CIRCLE('',#9806,0.5);
#3801=CIRCLE('',#9808,0.8);
#3802=CIRCLE('',#9811,0.5);
#4449=VERTEX_POINT('',#15110);
#4450=VERTEX_POINT('',#15112);
#4451=VERTEX_POINT('',#15117);
#4452=VERTEX_POINT('',#15119);
#4453=VERTEX_POINT('',#15122);
#4454=VERTEX_POINT('',#15127);
#5380=EDGE_CURVE('',#4449,#4449,#3797,.T.);
#5381=EDGE_CURVE('',#4449,#4450,#2881,.T.);
#5382=EDGE_CURVE('',#4450,#4450,#3798,.T.);
#5383=EDGE_CURVE('',#4451,#4451,#3799,.T.);
#5384=EDGE_CURVE('',#4452,#4452,#3800,.T.);
#5385=EDGE_CURVE('',#4451,#4453,#2882,.T.);
#5386=EDGE_CURVE('',#4453,#4453,#3801,.T.);
#5387=EDGE_CURVE('',#4454,#4454,#3802,.T.);
#5388=EDGE_CURVE('',#4454,#4452,#2883,.T.);
#7139=ORIENTED_EDGE('',*,*,#5380,.F.);
#7140=ORIENTED_EDGE('',*,*,#5381,.T.);
#7141=ORIENTED_EDGE('',*,*,#5382,.F.);
#7142=ORIENTED_EDGE('',*,*,#5381,.F.);
#7143=ORIENTED_EDGE('',*,*,#5380,.T.);
#7144=ORIENTED_EDGE('',*,*,#5383,.T.);
#7145=ORIENTED_EDGE('',*,*,#5384,.F.);
#7146=ORIENTED_EDGE('',*,*,#5383,.F.);
#7147=ORIENTED_EDGE('',*,*,#5385,.T.);
#7148=ORIENTED_EDGE('',*,*,#5386,.T.);
#7149=ORIENTED_EDGE('',*,*,#5385,.F.);
#7150=ORIENTED_EDGE('',*,*,#5386,.F.);
#7151=ORIENTED_EDGE('',*,*,#5387,.F.);
#7152=ORIENTED_EDGE('',*,*,#5388,.T.);
#7153=ORIENTED_EDGE('',*,*,#5384,.T.);
#7154=ORIENTED_EDGE('',*,*,#5388,.F.);
#7155=ORIENTED_EDGE('',*,*,#5387,.T.);
#7156=ORIENTED_EDGE('',*,*,#5382,.T.);
#7804=CYLINDRICAL_SURFACE('',#9800,0.165);
#7805=CYLINDRICAL_SURFACE('',#9807,0.8);
#7806=CYLINDRICAL_SURFACE('',#9810,0.5);
#8208=ADVANCED_FACE('',(#1605),#7804,.F.);
#8209=ADVANCED_FACE('',(#1606),#1177,.T.);
#8210=ADVANCED_FACE('',(#1607,#947),#1178,.T.);
#8211=ADVANCED_FACE('',(#1608),#7805,.T.);
#8212=ADVANCED_FACE('',(#1609),#1179,.F.);
#8213=ADVANCED_FACE('',(#1610),#7806,.T.);
#8214=ADVANCED_FACE('',(#1611,#948),#1180,.T.);
#8401=CLOSED_SHELL('',(#8208,#8209,#8210,#8211,#8212,#8213,#8214));
#9799=AXIS2_PLACEMENT_3D('',#15108,#12106,#12107);
#9800=AXIS2_PLACEMENT_3D('',#15109,#12108,#12109);
#9801=AXIS2_PLACEMENT_3D('',#15111,#12110,#12111);
#9802=AXIS2_PLACEMENT_3D('',#15114,#12113,#12114);
#9803=AXIS2_PLACEMENT_3D('',#15115,#12115,#12116);
#9804=AXIS2_PLACEMENT_3D('',#15116,#12117,#12118);
#9805=AXIS2_PLACEMENT_3D('',#15118,#12119,#12120);
#9806=AXIS2_PLACEMENT_3D('',#15120,#12121,#12122);
#9807=AXIS2_PLACEMENT_3D('',#15121,#12123,#12124);
#9808=AXIS2_PLACEMENT_3D('',#15124,#12126,#12127);
#9809=AXIS2_PLACEMENT_3D('',#15125,#12128,#12129);
#9810=AXIS2_PLACEMENT_3D('',#15126,#12130,#12131);
#9811=AXIS2_PLACEMENT_3D('',#15128,#12132,#12133);
#9812=AXIS2_PLACEMENT_3D('',#15130,#12135,#12136);
#12106=DIRECTION('axis',(0.,0.,1.));
#12107=DIRECTION('refdir',(1.,0.,0.));
#12108=DIRECTION('center_axis',(0.,1.,0.));
#12109=DIRECTION('ref_axis',(1.,0.,0.));
#12110=DIRECTION('center_axis',(0.,1.,0.));
#12111=DIRECTION('ref_axis',(1.,0.,0.));
#12112=DIRECTION('',(0.,1.,0.));
#12113=DIRECTION('center_axis',(0.,-1.,0.));
#12114=DIRECTION('ref_axis',(1.,0.,0.));
#12115=DIRECTION('center_axis',(0.,1.,0.));
#12116=DIRECTION('ref_axis',(1.,0.,0.));
#12117=DIRECTION('center_axis',(0.,1.,0.));
#12118=DIRECTION('ref_axis',(1.,0.,0.));
#12119=DIRECTION('center_axis',(0.,1.,0.));
#12120=DIRECTION('ref_axis',(1.,0.,0.));
#12121=DIRECTION('center_axis',(0.,1.,0.));
#12122=DIRECTION('ref_axis',(1.,0.,0.));
#12123=DIRECTION('center_axis',(0.,1.,0.));
#12124=DIRECTION('ref_axis',(1.,0.,0.));
#12125=DIRECTION('',(0.,-1.,0.));
#12126=DIRECTION('center_axis',(0.,1.,0.));
#12127=DIRECTION('ref_axis',(1.,0.,0.));
#12128=DIRECTION('center_axis',(0.,1.,0.));
#12129=DIRECTION('ref_axis',(1.,0.,0.));
#12130=DIRECTION('center_axis',(0.,1.,0.));
#12131=DIRECTION('ref_axis',(1.,0.,0.));
#12132=DIRECTION('center_axis',(0.,1.,0.));
#12133=DIRECTION('ref_axis',(1.,0.,0.));
#12134=DIRECTION('',(0.,-1.,0.));
#12135=DIRECTION('center_axis',(0.,1.,0.));
#12136=DIRECTION('ref_axis',(1.,0.,0.));
#15108=CARTESIAN_POINT('',(0.,0.,0.));
#15109=CARTESIAN_POINT('Origin',(0.,15.2,3.5));
#15110=CARTESIAN_POINT('',(-0.165,15.2,3.5));
#15111=CARTESIAN_POINT('Origin',(0.,15.2,3.5));
#15112=CARTESIAN_POINT('',(-0.165,16.3,3.5));
#15113=CARTESIAN_POINT('',(-0.165,15.2,3.5));
#15114=CARTESIAN_POINT('Origin',(0.,16.3,3.5));
#15115=CARTESIAN_POINT('Origin',(0.,15.2,3.5));
#15116=CARTESIAN_POINT('Origin',(0.,13.7,3.5));
#15117=CARTESIAN_POINT('',(-0.8,13.7,3.5));
#15118=CARTESIAN_POINT('Origin',(0.,13.7,3.5));
#15119=CARTESIAN_POINT('',(-0.5,13.7,3.5));
#15120=CARTESIAN_POINT('Origin',(0.,13.7,3.5));
#15121=CARTESIAN_POINT('Origin',(0.,13.3,3.5));
#15122=CARTESIAN_POINT('',(-0.8,13.3,3.5));
#15123=CARTESIAN_POINT('',(-0.8,13.3,3.5));
#15124=CARTESIAN_POINT('Origin',(0.,13.3,3.5));
#15125=CARTESIAN_POINT('Origin',(0.,13.3,3.5));
#15126=CARTESIAN_POINT('Origin',(0.,13.7,3.5));
#15127=CARTESIAN_POINT('',(-0.5,16.3,3.5));
#15128=CARTESIAN_POINT('Origin',(0.,16.3,3.5));
#15129=CARTESIAN_POINT('',(-0.5,13.7,3.5));
#15130=CARTESIAN_POINT('Origin',(0.,16.3,3.5));
#16184=UNCERTAINTY_MEASURE_WITH_UNIT(LENGTH_MEASURE(0.001),#16282,
'DISTANCE_ACCURACY_VALUE',
'Maximum model space distance between geometric entities at asserted c
onnectivities');
#16212=UNCERTAINTY_MEASURE_WITH_UNIT(LENGTH_MEASURE(0.001),#16282,
'DISTANCE_ACCURACY_VALUE',
'Maximum model space distance between geometric entities at asserted c
onnectivities');
#16253=(
GEOMETRIC_REPRESENTATION_CONTEXT(3)
GLOBAL_UNCERTAINTY_ASSIGNED_CONTEXT((#16184))
GLOBAL_UNIT_ASSIGNED_CONTEXT((#16282,#16284,#16285))
REPRESENTATION_CONTEXT('','3D')
);
#16281=(
GEOMETRIC_REPRESENTATION_CONTEXT(3)
GLOBAL_UNCERTAINTY_ASSIGNED_CONTEXT((#16212))
GLOBAL_UNIT_ASSIGNED_CONTEXT((#16282,#16284,#16285))
REPRESENTATION_CONTEXT('','3D')
);
#16282=(
LENGTH_UNIT()
NAMED_UNIT(*)
SI_UNIT(.CENTI.,.METRE.)
);
#16284=(
NAMED_UNIT(*)
PLANE_ANGLE_UNIT()
SI_UNIT($,.RADIAN.)
);
#16285=(
NAMED_UNIT(*)
SI_UNIT($,.STERADIAN.)
SOLID_ANGLE_UNIT()
);
#16326=SHAPE_DEFINITION_REPRESENTATION(#16420,#16559);
#16420=PRODUCT_DEFINITION_SHAPE('',$,#16628);
#16559=SHAPE_REPRESENTATION('',(#9799),#16253);
#16587=PRODUCT_DEFINITION_CONTEXT('part definition',#16793,'design');
#16628=PRODUCT_DEFINITION('Roller axle (3)','Roller axle (3)',#16696,#16587);
#16696=PRODUCT_DEFINITION_FORMATION('',$,#16835);
#16793=APPLICATION_CONTEXT(
'Core Data for Automotive Mechanical Design Process');
#16794=PRODUCT_CONTEXT('part definition',#16793,'mechanical');
#16835=PRODUCT('Roller axle (3)','Roller axle (3)','Roller axle (3)',(#16794));
#16926=COLOUR_RGB('Grey',0.48,0.52,0.57);
#16927=FILL_AREA_STYLE_COLOUR('',#16926);
#16928=FILL_AREA_STYLE('',(#16927));
#16929=SURFACE_STYLE_FILL_AREA(#16928);
#16930=SURFACE_SIDE_STYLE('',(#16929));
#16931=SURFACE_STYLE_USAGE(.BOTH.,#16930);
#16932=PRESENTATION_STYLE_ASSIGNMENT((#16931));
ENDSEC;
END-ISO-10303-21;
